ISO-10303-21;
HEADER;
/* Generated by software containing ST-Developer
 * from STEP Tools, Inc. (www.steptools.com) 
 */

FILE_DESCRIPTION(
/* description */ (''),
/* implementation_level */ '2;1');

FILE_NAME(
/* name */ 'PACKING_GLAND.step',
/* time_stamp */ '2026-10-04T02:10:06-07:00',
/* author */ (''),
/* organization */ (''),
/* preprocessor_version */ 'ST-DEVELOPER v20.2',
/* originating_system */ 'Autodesk Translation Framework v15.15.0.0',
/* authorisation */ '');

FILE_SCHEMA (('AUTOMOTIVE_DESIGN { 1 0 10303 214 3 1 1 }'));
ENDSEC;

DATA;
#10=MECHANICAL_DESIGN_GEOMETRIC_PRESENTATION_REPRESENTATION('',(#147),#9668);
#125=SHAPE_REPRESENTATION_RELATIONSHIP('SRR','None',#9718,#136);
#136=ADVANCED_BREP_SHAPE_REPRESENTATION('',(#158),#9663);
#147=STYLED_ITEM('',(#9775),#158);
#158=MANIFOLD_SOLID_BREP('Body1',#3887);
#175=CONICAL_SURFACE('',#4291,10.,1.10714871779409);
#254=FACE_BOUND('',#1214,.T.);
#255=FACE_BOUND('',#1217,.T.);
#320=PLANE('',#4283);
#321=PLANE('',#4287);
#484=LINE('',#6851,#675);
#485=LINE('',#6859,#676);
#486=LINE('',#6866,#677);
#487=LINE('',#6868,#678);
#675=VECTOR('',#5118,10.);
#676=VECTOR('',#5129,22.0000000000001);
#677=VECTOR('',#5138,18.);
#678=VECTOR('',#5141,10.);
#801=CYLINDRICAL_SURFACE('',#4280,10.);
#802=CYLINDRICAL_SURFACE('',#4285,22.0000000000001);
#803=CYLINDRICAL_SURFACE('',#4289,18.);
#930=FACE_OUTER_BOUND('',#1212,.T.);
#931=FACE_OUTER_BOUND('',#1213,.T.);
#932=FACE_OUTER_BOUND('',#1215,.T.);
#933=FACE_OUTER_BOUND('',#1216,.T.);
#934=FACE_OUTER_BOUND('',#1218,.T.);
#935=FACE_OUTER_BOUND('',#1219,.T.);
#1212=EDGE_LOOP('',(#3119,#3120,#3121,#3122));
#1213=EDGE_LOOP('',(#3123));
#1214=EDGE_LOOP('',(#3124));
#1215=EDGE_LOOP('',(#3125,#3126,#3127,#3128));
#1216=EDGE_LOOP('',(#3129));
#1217=EDGE_LOOP('',(#3130));
#1218=EDGE_LOOP('',(#3131,#3132,#3133,#3134));
#1219=EDGE_LOOP('',(#3135,#3136,#3137,#3138));
#1565=CIRCLE('',#4281,10.0000000000001);
#1566=CIRCLE('',#4282,10.);
#1567=CIRCLE('',#4284,22.0000000000001);
#1568=CIRCLE('',#4286,22.);
#1569=CIRCLE('',#4288,18.);
#1570=CIRCLE('',#4290,18.);
#1831=VERTEX_POINT('',#6848);
#1832=VERTEX_POINT('',#6850);
#1833=VERTEX_POINT('',#6854);
#1834=VERTEX_POINT('',#6857);
#1835=VERTEX_POINT('',#6861);
#1836=VERTEX_POINT('',#6864);
#2283=EDGE_CURVE('',#1831,#1831,#1565,.T.);
#2284=EDGE_CURVE('',#1831,#1832,#484,.T.);
#2285=EDGE_CURVE('',#1832,#1832,#1566,.T.);
#2286=EDGE_CURVE('',#1833,#1833,#1567,.T.);
#2287=EDGE_CURVE('',#1834,#1834,#1568,.T.);
#2288=EDGE_CURVE('',#1834,#1833,#485,.T.);
#2289=EDGE_CURVE('',#1835,#1835,#1569,.T.);
#2290=EDGE_CURVE('',#1836,#1836,#1570,.T.);
#2291=EDGE_CURVE('',#1836,#1835,#486,.T.);
#2292=EDGE_CURVE('',#1832,#1836,#487,.T.);
#3119=ORIENTED_EDGE('',*,*,#2283,.F.);
#3120=ORIENTED_EDGE('',*,*,#2284,.T.);
#3121=ORIENTED_EDGE('',*,*,#2285,.T.);
#3122=ORIENTED_EDGE('',*,*,#2284,.F.);
#3123=ORIENTED_EDGE('',*,*,#2286,.F.);
#3124=ORIENTED_EDGE('',*,*,#2283,.T.);
#3125=ORIENTED_EDGE('',*,*,#2287,.F.);
#3126=ORIENTED_EDGE('',*,*,#2288,.T.);
#3127=ORIENTED_EDGE('',*,*,#2286,.T.);
#3128=ORIENTED_EDGE('',*,*,#2288,.F.);
#3129=ORIENTED_EDGE('',*,*,#2287,.T.);
#3130=ORIENTED_EDGE('',*,*,#2289,.F.);
#3131=ORIENTED_EDGE('',*,*,#2290,.F.);
#3132=ORIENTED_EDGE('',*,*,#2291,.T.);
#3133=ORIENTED_EDGE('',*,*,#2289,.T.);
#3134=ORIENTED_EDGE('',*,*,#2291,.F.);
#3135=ORIENTED_EDGE('',*,*,#2285,.F.);
#3136=ORIENTED_EDGE('',*,*,#2292,.T.);
#3137=ORIENTED_EDGE('',*,*,#2290,.T.);
#3138=ORIENTED_EDGE('',*,*,#2292,.F.);
#3778=ADVANCED_FACE('',(#930),#801,.F.);
#3779=ADVANCED_FACE('',(#931,#254),#320,.T.);
#3780=ADVANCED_FACE('',(#932),#802,.T.);
#3781=ADVANCED_FACE('',(#933,#255),#321,.T.);
#3782=ADVANCED_FACE('',(#934),#803,.T.);
#3783=ADVANCED_FACE('',(#935),#175,.F.);
#3887=CLOSED_SHELL('',(#3778,#3779,#3780,#3781,#3782,#3783));
#4279=AXIS2_PLACEMENT_3D('',#6846,#5112,#5113);
#4280=AXIS2_PLACEMENT_3D('',#6847,#5114,#5115);
#4281=AXIS2_PLACEMENT_3D('',#6849,#5116,#5117);
#4282=AXIS2_PLACEMENT_3D('',#6852,#5119,#5120);
#4283=AXIS2_PLACEMENT_3D('',#6853,#5121,#5122);
#4284=AXIS2_PLACEMENT_3D('',#6855,#5123,#5124);
#4285=AXIS2_PLACEMENT_3D('',#6856,#5125,#5126);
#4286=AXIS2_PLACEMENT_3D('',#6858,#5127,#5128);
#4287=AXIS2_PLACEMENT_3D('',#6860,#5130,#5131);
#4288=AXIS2_PLACEMENT_3D('',#6862,#5132,#5133);
#4289=AXIS2_PLACEMENT_3D('',#6863,#5134,#5135);
#4290=AXIS2_PLACEMENT_3D('',#6865,#5136,#5137);
#4291=AXIS2_PLACEMENT_3D('',#6867,#5139,#5140);
#5112=DIRECTION('axis',(0.,0.,1.));
#5113=DIRECTION('refdir',(1.,0.,0.));
#5114=DIRECTION('center_axis',(3.43024899888577E-15,-1.,0.));
#5115=DIRECTION('ref_axis',(1.,3.43024899888577E-15,0.));
#5116=DIRECTION('center_axis',(3.43024899888577E-15,-1.,0.));
#5117=DIRECTION('ref_axis',(1.,3.43024899888577E-15,0.));
#5118=DIRECTION('',(3.43024899888577E-15,-1.,0.));
#5119=DIRECTION('center_axis',(3.43024899888577E-15,-1.,0.));
#5120=DIRECTION('ref_axis',(1.,3.43024899888577E-15,0.));
#5121=DIRECTION('center_axis',(-3.43024899888577E-15,1.,0.));
#5122=DIRECTION('ref_axis',(0.,0.,1.));
#5123=DIRECTION('center_axis',(3.43024899888577E-15,-1.,0.));
#5124=DIRECTION('ref_axis',(1.,3.43024899888577E-15,0.));
#5125=DIRECTION('center_axis',(3.43024899888577E-15,-1.,0.));
#5126=DIRECTION('ref_axis',(1.,3.43024899888577E-15,0.));
#5127=DIRECTION('center_axis',(3.43024899888577E-15,-1.,0.));
#5128=DIRECTION('ref_axis',(1.,3.43024899888577E-15,0.));
#5129=DIRECTION('',(-3.43024899888577E-15,1.,0.));
#5130=DIRECTION('center_axis',(3.43024899888577E-15,-1.,0.));
#5131=DIRECTION('ref_axis',(0.,0.,-1.));
#5132=DIRECTION('center_axis',(3.43024899888577E-15,-1.,0.));
#5133=DIRECTION('ref_axis',(1.,3.43024899888577E-15,0.));
#5134=DIRECTION('center_axis',(3.43024899888577E-15,-1.,0.));
#5135=DIRECTION('ref_axis',(1.,3.43024899888577E-15,0.));
#5136=DIRECTION('center_axis',(3.43024899888577E-15,-1.,0.));
#5137=DIRECTION('ref_axis',(1.,3.43024899888577E-15,0.));
#5138=DIRECTION('',(-3.43024899888577E-15,1.,0.));
#5139=DIRECTION('center_axis',(3.43024899888577E-15,-1.,0.));
#5140=DIRECTION('ref_axis',(1.,3.43024899888577E-15,0.));
#5141=DIRECTION('',(-0.894427190999914,-0.447213595499962,-1.0953573965284E-16));
#6846=CARTESIAN_POINT('',(0.,0.,0.));
#6847=CARTESIAN_POINT('Origin',(1.66027257158657E-12,-484.009345130884,
0.));
#6848=CARTESIAN_POINT('',(-10.0000000000001,18.,-1.22464679914736E-15));
#6849=CARTESIAN_POINT('Origin',(-6.17444819799439E-14,18.,0.));
#6850=CARTESIAN_POINT('',(-10.0000000000001,3.99999999999991,-1.22464679914736E-15));
#6851=CARTESIAN_POINT('',(-9.99999999999839,-484.009345130884,-1.22464679914736E-15));
#6852=CARTESIAN_POINT('Origin',(-1.37209959955432E-14,3.99999999999995,
0.));
#6853=CARTESIAN_POINT('Origin',(10.,18.,0.));
#6854=CARTESIAN_POINT('',(-22.0000000000001,17.9999999999998,-2.69422295812418E-15));
#6855=CARTESIAN_POINT('Origin',(-6.17444819799435E-14,17.9999999999999,
0.));
#6856=CARTESIAN_POINT('Origin',(1.66027257158657E-12,-484.009345130884,
0.));
#6857=CARTESIAN_POINT('',(-22.0000000000001,15.9999999999998,-2.69422295812418E-15));
#6858=CARTESIAN_POINT('Origin',(-5.48839839821719E-14,15.9999999999998,
0.));
#6859=CARTESIAN_POINT('',(-21.9999999999984,-484.009345130884,-2.69422295812418E-15));
#6860=CARTESIAN_POINT('Origin',(22.,16.,0.));
#6861=CARTESIAN_POINT('',(-18.0000000000001,15.9999999999998,-2.20436423846524E-15));
#6862=CARTESIAN_POINT('Origin',(-5.48839839821719E-14,15.9999999999998,
0.));
#6863=CARTESIAN_POINT('Origin',(1.66027257158657E-12,-484.009345130884,
0.));
#6864=CARTESIAN_POINT('',(-18.,-1.4210854715202E-13,-2.20436423846524E-15));
#6865=CARTESIAN_POINT('Origin',(0.,-5.55111512312578E-14,0.));
#6866=CARTESIAN_POINT('',(-17.9999999999984,-484.009345130884,-2.20436423846524E-15));
#6867=CARTESIAN_POINT('Origin',(-1.37209959955432E-14,3.99999999999995,
0.));
#6868=CARTESIAN_POINT('',(-10.,3.99999999999991,-1.22464679914736E-15));
#9650=UNCERTAINTY_MEASURE_WITH_UNIT(LENGTH_MEASURE(0.01),#9669,
'DISTANCE_ACCURACY_VALUE',
'Maximum model space distance between geometric entities at asserted c
onnectivities');
#9655=UNCERTAINTY_MEASURE_WITH_UNIT(LENGTH_MEASURE(0.01),#9669,
'DISTANCE_ACCURACY_VALUE',
'Maximum model space distance between geometric entities at asserted c
onnectivities');
#9663=(
GEOMETRIC_REPRESENTATION_CONTEXT(3)
GLOBAL_UNCERTAINTY_ASSIGNED_CONTEXT((#9650))
GLOBAL_UNIT_ASSIGNED_CONTEXT((#9669,#9671,#9672))
REPRESENTATION_CONTEXT('','3D')
);
#9668=(
GEOMETRIC_REPRESENTATION_CONTEXT(3)
GLOBAL_UNCERTAINTY_ASSIGNED_CONTEXT((#9655))
GLOBAL_UNIT_ASSIGNED_CONTEXT((#9669,#9671,#9672))
REPRESENTATION_CONTEXT('','3D')
);
#9669=(
LENGTH_UNIT()
NAMED_UNIT(*)
SI_UNIT(.MILLI.,.METRE.)
);
#9671=(
NAMED_UNIT(*)
PLANE_ANGLE_UNIT()
SI_UNIT($,.RADIAN.)
);
#9672=(
NAMED_UNIT(*)
SI_UNIT($,.STERADIAN.)
SOLID_ANGLE_UNIT()
);
#9680=SHAPE_DEFINITION_REPRESENTATION(#9692,#9718);
#9692=PRODUCT_DEFINITION_SHAPE('',$,#9731);
#9718=SHAPE_REPRESENTATION('',(#4279),#9663);
#9723=PRODUCT_DEFINITION_CONTEXT('part definition',#9761,'design');
#9731=PRODUCT_DEFINITION('2026-10-04-08-13-48-886','PACKING_GLAND',#9743,
#9723);
#9743=PRODUCT_DEFINITION_FORMATION('',$,#9770);
#9761=APPLICATION_CONTEXT(
'Core Data for Automotive Mechanical Design Process');
#9762=PRODUCT_CONTEXT('part definition',#9761,'mechanical');
#9770=PRODUCT('2026-10-04-08-13-48-886','PACKING_GLAND','PART',(#9762));
#9775=PRESENTATION_STYLE_ASSIGNMENT((#9776));
#9776=SURFACE_STYLE_USAGE(.BOTH.,#9777);
#9777=SURFACE_SIDE_STYLE('',(#9778));
#9778=SURFACE_STYLE_FILL_AREA(#9779);
#9779=FILL_AREA_STYLE('Steel - Satin',(#9780));
#9780=FILL_AREA_STYLE_COLOUR('Steel - Satin',#9781);
#9781=COLOUR_RGB('Steel - Satin', 0.09019608, 0.27058824, 0.51372549);
ENDSEC;
END-ISO-10303-21;
